ISO-10303-21;
HEADER;
/* Generated by software containing ST-Developer
 * from STEP Tools, Inc. (www.steptools.com) 
 */

FILE_DESCRIPTION(
/* description */ ('Two-stage gear reducer in split housing'),
/* implementation_level */ '2;1');

FILE_NAME(
/* name */ 'Socket Set Screw - M5x8.step',
/* time_stamp */ '2026-10-28T03:22:31-07:00',
/* author */ (''),
/* organization */ (''),
/* preprocessor_version */ 'ST-DEVELOPER v20.2',
/* originating_system */ 'Autodesk Translation Framework v15.17.0.0',
/* authorisation */ '');

FILE_SCHEMA (('AUTOMOTIVE_DESIGN { 1 0 10303 214 3 1 1 }'));
ENDSEC;

DATA;
#10=MECHANICAL_DESIGN_GEOMETRIC_PRESENTATION_REPRESENTATION('',(#1302),#73366);
#1116=CONICAL_SURFACE('',#18227,0.235,0.785398163397448);
#1117=CONICAL_SURFACE('',#18231,0.2125,0.785398163397448);
#1175=SHAPE_REPRESENTATION_RELATIONSHIP('SRR','None',#73667,#1231);
#1231=ADVANCED_BREP_SHAPE_REPRESENTATION('',(#1371),#73363);
#1302=STYLED_ITEM('',(#73995),#1371);
#1371=MANIFOLD_SOLID_BREP('Body1',#16192);
#1598=FACE_BOUND('',#3870,.T.);
#1937=PLANE('',#18218);
#1938=PLANE('',#18219);
#1939=PLANE('',#18220);
#1940=PLANE('',#18221);
#1941=PLANE('',#18222);
#1942=PLANE('',#18223);
#1943=PLANE('',#18224);
#1944=PLANE('',#18225);
#1945=PLANE('',#18233);
#2725=FACE_OUTER_BOUND('',#3862,.T.);
#2726=FACE_OUTER_BOUND('',#3863,.T.);
#2727=FACE_OUTER_BOUND('',#3864,.T.);
#2728=FACE_OUTER_BOUND('',#3865,.T.);
#2729=FACE_OUTER_BOUND('',#3866,.T.);
#2730=FACE_OUTER_BOUND('',#3867,.T.);
#2731=FACE_OUTER_BOUND('',#3868,.T.);
#2732=FACE_OUTER_BOUND('',#3869,.T.);
#2733=FACE_OUTER_BOUND('',#3871,.T.);
#2734=FACE_OUTER_BOUND('',#3872,.T.);
#2735=FACE_OUTER_BOUND('',#3873,.T.);
#2736=FACE_OUTER_BOUND('',#3874,.T.);
#3862=EDGE_LOOP('',(#13819,#13820,#13821,#13822));
#3863=EDGE_LOOP('',(#13823,#13824,#13825,#13826));
#3864=EDGE_LOOP('',(#13827,#13828,#13829,#13830));
#3865=EDGE_LOOP('',(#13831,#13832,#13833,#13834));
#3866=EDGE_LOOP('',(#13835,#13836,#13837,#13838));
#3867=EDGE_LOOP('',(#13839,#13840,#13841,#13842));
#3868=EDGE_LOOP('',(#13843,#13844,#13845,#13846,#13847,#13848));
#3869=EDGE_LOOP('',(#13849));
#3870=EDGE_LOOP('',(#13850,#13851,#13852,#13853,#13854,#13855));
#3871=EDGE_LOOP('',(#13856,#13857,#13858,#13859));
#3872=EDGE_LOOP('',(#13860,#13861,#13862,#13863));
#3873=EDGE_LOOP('',(#13864,#13865,#13866,#13867));
#3874=EDGE_LOOP('',(#13868));
#4864=LINE('',#49544,#5888);
#4865=LINE('',#49546,#5889);
#4866=LINE('',#49548,#5890);
#4867=LINE('',#49549,#5891);
#4868=LINE('',#49552,#5892);
#4869=LINE('',#49554,#5893);
#4870=LINE('',#49555,#5894);
#4871=LINE('',#49558,#5895);
#4872=LINE('',#49560,#5896);
#4873=LINE('',#49561,#5897);
#4874=LINE('',#49564,#5898);
#4875=LINE('',#49566,#5899);
#4876=LINE('',#49567,#5900);
#4877=LINE('',#49570,#5901);
#4878=LINE('',#49572,#5902);
#4879=LINE('',#49573,#5903);
#4880=LINE('',#49575,#5904);
#4881=LINE('',#49576,#5905);
#4882=LINE('',#49584,#5906);
#4883=LINE('',#49588,#5907);
#4884=LINE('',#49592,#5908);
#5888=VECTOR('',#22080,1.);
#5889=VECTOR('',#22081,1.);
#5890=VECTOR('',#22082,1.);
#5891=VECTOR('',#22083,1.);
#5892=VECTOR('',#22086,1.);
#5893=VECTOR('',#22087,1.);
#5894=VECTOR('',#22088,1.);
#5895=VECTOR('',#22091,1.);
#5896=VECTOR('',#22092,1.);
#5897=VECTOR('',#22093,1.);
#5898=VECTOR('',#22096,1.);
#5899=VECTOR('',#22097,1.);
#5900=VECTOR('',#22098,1.);
#5901=VECTOR('',#22101,1.);
#5902=VECTOR('',#22102,1.);
#5903=VECTOR('',#22103,1.);
#5904=VECTOR('',#22106,1.);
#5905=VECTOR('',#22107,1.);
#5906=VECTOR('',#22118,0.235);
#5907=VECTOR('',#22123,0.25);
#5908=VECTOR('',#22128,0.2125);
#6736=CIRCLE('',#18226,0.22);
#6737=CIRCLE('',#18228,0.24505);
#6738=CIRCLE('',#18230,0.24505);
#6739=CIRCLE('',#18232,0.175);
#7945=VERTEX_POINT('',#49542);
#7946=VERTEX_POINT('',#49543);
#7947=VERTEX_POINT('',#49545);
#7948=VERTEX_POINT('',#49547);
#7949=VERTEX_POINT('',#49551);
#7950=VERTEX_POINT('',#49553);
#7951=VERTEX_POINT('',#49557);
#7952=VERTEX_POINT('',#49559);
#7953=VERTEX_POINT('',#49563);
#7954=VERTEX_POINT('',#49565);
#7955=VERTEX_POINT('',#49569);
#7956=VERTEX_POINT('',#49571);
#7957=VERTEX_POINT('',#49579);
#7958=VERTEX_POINT('',#49582);
#7959=VERTEX_POINT('',#49586);
#7960=VERTEX_POINT('',#49590);
#9963=EDGE_CURVE('',#7945,#7946,#4864,.T.);
#9964=EDGE_CURVE('',#7945,#7947,#4865,.T.);
#9965=EDGE_CURVE('',#7947,#7948,#4866,.T.);
#9966=EDGE_CURVE('',#7946,#7948,#4867,.T.);
#9967=EDGE_CURVE('',#7949,#7945,#4868,.T.);
#9968=EDGE_CURVE('',#7949,#7950,#4869,.T.);
#9969=EDGE_CURVE('',#7950,#7947,#4870,.T.);
#9970=EDGE_CURVE('',#7951,#7949,#4871,.T.);
#9971=EDGE_CURVE('',#7951,#7952,#4872,.T.);
#9972=EDGE_CURVE('',#7952,#7950,#4873,.T.);
#9973=EDGE_CURVE('',#7953,#7951,#4874,.T.);
#9974=EDGE_CURVE('',#7953,#7954,#4875,.T.);
#9975=EDGE_CURVE('',#7954,#7952,#4876,.T.);
#9976=EDGE_CURVE('',#7955,#7953,#4877,.T.);
#9977=EDGE_CURVE('',#7955,#7956,#4878,.T.);
#9978=EDGE_CURVE('',#7956,#7954,#4879,.T.);
#9979=EDGE_CURVE('',#7946,#7955,#4880,.T.);
#9980=EDGE_CURVE('',#7948,#7956,#4881,.T.);
#9981=EDGE_CURVE('',#7957,#7957,#6736,.T.);
#9982=EDGE_CURVE('',#7958,#7958,#6737,.T.);
#9983=EDGE_CURVE('',#7958,#7957,#4882,.T.);
#9984=EDGE_CURVE('',#7959,#7959,#6738,.F.);
#9985=EDGE_CURVE('',#7959,#7958,#4883,.T.);
#9986=EDGE_CURVE('',#7960,#7960,#6739,.T.);
#9987=EDGE_CURVE('',#7960,#7959,#4884,.T.);
#13819=ORIENTED_EDGE('',*,*,#9963,.F.);
#13820=ORIENTED_EDGE('',*,*,#9964,.T.);
#13821=ORIENTED_EDGE('',*,*,#9965,.T.);
#13822=ORIENTED_EDGE('',*,*,#9966,.F.);
#13823=ORIENTED_EDGE('',*,*,#9967,.F.);
#13824=ORIENTED_EDGE('',*,*,#9968,.T.);
#13825=ORIENTED_EDGE('',*,*,#9969,.T.);
#13826=ORIENTED_EDGE('',*,*,#9964,.F.);
#13827=ORIENTED_EDGE('',*,*,#9970,.F.);
#13828=ORIENTED_EDGE('',*,*,#9971,.T.);
#13829=ORIENTED_EDGE('',*,*,#9972,.T.);
#13830=ORIENTED_EDGE('',*,*,#9968,.F.);
#13831=ORIENTED_EDGE('',*,*,#9973,.F.);
#13832=ORIENTED_EDGE('',*,*,#9974,.T.);
#13833=ORIENTED_EDGE('',*,*,#9975,.T.);
#13834=ORIENTED_EDGE('',*,*,#9971,.F.);
#13835=ORIENTED_EDGE('',*,*,#9976,.F.);
#13836=ORIENTED_EDGE('',*,*,#9977,.T.);
#13837=ORIENTED_EDGE('',*,*,#9978,.T.);
#13838=ORIENTED_EDGE('',*,*,#9974,.F.);
#13839=ORIENTED_EDGE('',*,*,#9979,.F.);
#13840=ORIENTED_EDGE('',*,*,#9966,.T.);
#13841=ORIENTED_EDGE('',*,*,#9980,.T.);
#13842=ORIENTED_EDGE('',*,*,#9977,.F.);
#13843=ORIENTED_EDGE('',*,*,#9980,.F.);
#13844=ORIENTED_EDGE('',*,*,#9965,.F.);
#13845=ORIENTED_EDGE('',*,*,#9969,.F.);
#13846=ORIENTED_EDGE('',*,*,#9972,.F.);
#13847=ORIENTED_EDGE('',*,*,#9975,.F.);
#13848=ORIENTED_EDGE('',*,*,#9978,.F.);
#13849=ORIENTED_EDGE('',*,*,#9981,.F.);
#13850=ORIENTED_EDGE('',*,*,#9963,.T.);
#13851=ORIENTED_EDGE('',*,*,#9979,.T.);
#13852=ORIENTED_EDGE('',*,*,#9976,.T.);
#13853=ORIENTED_EDGE('',*,*,#9973,.T.);
#13854=ORIENTED_EDGE('',*,*,#9970,.T.);
#13855=ORIENTED_EDGE('',*,*,#9967,.T.);
#13856=ORIENTED_EDGE('',*,*,#9982,.F.);
#13857=ORIENTED_EDGE('',*,*,#9983,.T.);
#13858=ORIENTED_EDGE('',*,*,#9981,.T.);
#13859=ORIENTED_EDGE('',*,*,#9983,.F.);
#13860=ORIENTED_EDGE('',*,*,#9984,.F.);
#13861=ORIENTED_EDGE('',*,*,#9985,.T.);
#13862=ORIENTED_EDGE('',*,*,#9982,.T.);
#13863=ORIENTED_EDGE('',*,*,#9985,.F.);
#13864=ORIENTED_EDGE('',*,*,#9986,.F.);
#13865=ORIENTED_EDGE('',*,*,#9987,.T.);
#13866=ORIENTED_EDGE('',*,*,#9984,.T.);
#13867=ORIENTED_EDGE('',*,*,#9987,.F.);
#13868=ORIENTED_EDGE('',*,*,#9986,.T.);
#15166=CYLINDRICAL_SURFACE('',#18229,0.24505);
#15932=ADVANCED_FACE('',(#2725),#1937,.F.);
#15933=ADVANCED_FACE('',(#2726),#1938,.F.);
#15934=ADVANCED_FACE('',(#2727),#1939,.F.);
#15935=ADVANCED_FACE('',(#2728),#1940,.F.);
#15936=ADVANCED_FACE('',(#2729),#1941,.F.);
#15937=ADVANCED_FACE('',(#2730),#1942,.F.);
#15938=ADVANCED_FACE('',(#2731),#1943,.F.);
#15939=ADVANCED_FACE('',(#2732,#1598),#1944,.T.);
#15940=ADVANCED_FACE('',(#2733),#1116,.T.);
#15941=ADVANCED_FACE('',(#2734),#15166,.T.);
#15942=ADVANCED_FACE('',(#2735),#1117,.T.);
#15943=ADVANCED_FACE('',(#2736),#1945,.T.);
#16192=CLOSED_SHELL('',(#15932,#15933,#15934,#15935,#15936,#15937,#15938,
#15939,#15940,#15941,#15942,#15943));
#18217=AXIS2_PLACEMENT_3D('',#49540,#22076,#22077);
#18218=AXIS2_PLACEMENT_3D('',#49541,#22078,#22079);
#18219=AXIS2_PLACEMENT_3D('',#49550,#22084,#22085);
#18220=AXIS2_PLACEMENT_3D('',#49556,#22089,#22090);
#18221=AXIS2_PLACEMENT_3D('',#49562,#22094,#22095);
#18222=AXIS2_PLACEMENT_3D('',#49568,#22099,#22100);
#18223=AXIS2_PLACEMENT_3D('',#49574,#22104,#22105);
#18224=AXIS2_PLACEMENT_3D('',#49577,#22108,#22109);
#18225=AXIS2_PLACEMENT_3D('',#49578,#22110,#22111);
#18226=AXIS2_PLACEMENT_3D('',#49580,#22112,#22113);
#18227=AXIS2_PLACEMENT_3D('',#49581,#22114,#22115);
#18228=AXIS2_PLACEMENT_3D('',#49583,#22116,#22117);
#18229=AXIS2_PLACEMENT_3D('',#49585,#22119,#22120);
#18230=AXIS2_PLACEMENT_3D('',#49587,#22121,#22122);
#18231=AXIS2_PLACEMENT_3D('',#49589,#22124,#22125);
#18232=AXIS2_PLACEMENT_3D('',#49591,#22126,#22127);
#18233=AXIS2_PLACEMENT_3D('',#49593,#22129,#22130);
#22076=DIRECTION('axis',(0.,0.,1.));
#22077=DIRECTION('refdir',(1.,0.,0.));
#22078=DIRECTION('center_axis',(0.866025403784439,0.,-0.5));
#22079=DIRECTION('ref_axis',(0.5,0.,0.866025403784439));
#22080=DIRECTION('',(0.5,0.,0.866025403784439));
#22081=DIRECTION('',(0.,-1.,0.));
#22082=DIRECTION('',(0.5,0.,0.866025403784439));
#22083=DIRECTION('',(0.,-1.,0.));
#22084=DIRECTION('center_axis',(1.92296268638356E-16,0.,-1.));
#22085=DIRECTION('ref_axis',(1.,0.,1.92296268638356E-16));
#22086=DIRECTION('',(1.,0.,1.92296268638356E-16));
#22087=DIRECTION('',(0.,-1.,0.));
#22088=DIRECTION('',(1.,0.,1.92296268638356E-16));
#22089=DIRECTION('center_axis',(-0.866025403784439,0.,-0.5));
#22090=DIRECTION('ref_axis',(0.5,0.,-0.866025403784439));
#22091=DIRECTION('',(0.5,0.,-0.866025403784439));
#22092=DIRECTION('',(0.,-1.,0.));
#22093=DIRECTION('',(0.5,0.,-0.866025403784438));
#22094=DIRECTION('center_axis',(-0.866025403784439,0.,0.5));
#22095=DIRECTION('ref_axis',(-0.5,0.,-0.866025403784439));
#22096=DIRECTION('',(-0.5,0.,-0.866025403784439));
#22097=DIRECTION('',(0.,-1.,0.));
#22098=DIRECTION('',(-0.5,0.,-0.866025403784439));
#22099=DIRECTION('center_axis',(-1.92296268638356E-16,0.,1.));
#22100=DIRECTION('ref_axis',(-1.,0.,-1.92296268638356E-16));
#22101=DIRECTION('',(-1.,0.,-1.92296268638356E-16));
#22102=DIRECTION('',(0.,-1.,0.));
#22103=DIRECTION('',(-1.,0.,-1.92296268638356E-16));
#22104=DIRECTION('center_axis',(0.866025403784439,0.,0.5));
#22105=DIRECTION('ref_axis',(-0.5,0.,0.866025403784439));
#22106=DIRECTION('',(-0.5,0.,0.866025403784439));
#22107=DIRECTION('',(-0.5,0.,0.866025403784439));
#22108=DIRECTION('center_axis',(0.,-1.,0.));
#22109=DIRECTION('ref_axis',(0.,0.,-1.));
#22110=DIRECTION('center_axis',(0.,1.,0.));
#22111=DIRECTION('ref_axis',(0.,0.,1.));
#22112=DIRECTION('center_axis',(0.,-1.,0.));
#22113=DIRECTION('ref_axis',(1.,0.,0.));
#22114=DIRECTION('center_axis',(0.,-1.,0.));
#22115=DIRECTION('ref_axis',(1.,0.,0.));
#22116=DIRECTION('center_axis',(0.,-1.,0.));
#22117=DIRECTION('ref_axis',(1.,0.,0.));
#22118=DIRECTION('',(0.707106781186547,0.707106781186548,8.65956056235493E-17));
#22119=DIRECTION('center_axis',(0.,-1.,0.));
#22120=DIRECTION('ref_axis',(1.,0.,0.));
#22121=DIRECTION('center_axis',(0.,1.,0.));
#22122=DIRECTION('ref_axis',(1.,0.,0.));
#22123=DIRECTION('',(0.,1.,0.));
#22124=DIRECTION('center_axis',(0.,1.,0.));
#22125=DIRECTION('ref_axis',(1.,0.,0.));
#22126=DIRECTION('center_axis',(0.,-1.,0.));
#22127=DIRECTION('ref_axis',(1.,0.,0.));
#22128=DIRECTION('',(-0.707106781186547,0.707106781186548,-8.65956056235493E-17));
#22129=DIRECTION('center_axis',(0.,-1.,0.));
#22130=DIRECTION('ref_axis',(0.,0.,-1.));
#49540=CARTESIAN_POINT('',(0.,0.,0.));
#49541=CARTESIAN_POINT('Origin',(0.0721687836487032,0.,-0.125));
#49542=CARTESIAN_POINT('',(0.0721687836487032,0.,-0.125));
#49543=CARTESIAN_POINT('',(0.144337567297406,0.,0.));
#49544=CARTESIAN_POINT('',(0.117710979560879,0.,-0.0461186027918559));
#49545=CARTESIAN_POINT('',(0.0721687836487032,-0.25,-0.125));
#49546=CARTESIAN_POINT('',(0.0721687836487032,0.,-0.125));
#49547=CARTESIAN_POINT('',(0.144337567297406,-0.25,0.));
#49548=CARTESIAN_POINT('',(0.144337567297406,-0.25,0.));
#49549=CARTESIAN_POINT('',(0.144337567297406,0.,0.));
#49550=CARTESIAN_POINT('Origin',(-0.0721687836487032,0.,-0.125));
#49551=CARTESIAN_POINT('',(-0.0721687836487032,0.,-0.125));
#49552=CARTESIAN_POINT('',(0.0739156081756484,0.,-0.125));
#49553=CARTESIAN_POINT('',(-0.0721687836487032,-0.25,-0.125));
#49554=CARTESIAN_POINT('',(-0.0721687836487032,0.,-0.125));
#49555=CARTESIAN_POINT('',(0.0721687836487032,-0.25,-0.125));
#49556=CARTESIAN_POINT('Origin',(-0.144337567297406,0.,-4.16333634234434E-17));
#49557=CARTESIAN_POINT('',(-0.144337567297406,0.,-1.76762539787485E-17));
#49558=CARTESIAN_POINT('',(-0.0987953713852306,0.,-0.0788813972081442));
#49559=CARTESIAN_POINT('',(-0.144337567297406,-0.25,-2.77555756156289E-17));
#49560=CARTESIAN_POINT('',(-0.144337567297406,0.,-1.76762539787485E-17));
#49561=CARTESIAN_POINT('',(-0.0721687836487032,-0.25,-0.125));
#49562=CARTESIAN_POINT('Origin',(-0.0721687836487033,0.,0.125));
#49563=CARTESIAN_POINT('',(-0.0721687836487033,0.,0.125));
#49564=CARTESIAN_POINT('',(-0.0627109795608791,0.,0.141381397208144));
#49565=CARTESIAN_POINT('',(-0.0721687836487033,-0.25,0.125));
#49566=CARTESIAN_POINT('',(-0.0721687836487033,0.,0.125));
#49567=CARTESIAN_POINT('',(-0.144337567297406,-0.25,-1.76762539787485E-17));
#49568=CARTESIAN_POINT('Origin',(0.0721687836487032,0.,0.125));
#49569=CARTESIAN_POINT('',(0.0721687836487032,0.,0.125));
#49570=CARTESIAN_POINT('',(0.146084391824352,0.,0.125));
#49571=CARTESIAN_POINT('',(0.0721687836487032,-0.25,0.125));
#49572=CARTESIAN_POINT('',(0.0721687836487032,0.,0.125));
#49573=CARTESIAN_POINT('',(-0.0721687836487033,-0.25,0.125));
#49574=CARTESIAN_POINT('Origin',(0.144337567297406,0.,0.));
#49575=CARTESIAN_POINT('',(0.153795371385231,0.,-0.0163813972081441));
#49576=CARTESIAN_POINT('',(0.0721687836487032,-0.25,0.125));
#49577=CARTESIAN_POINT('Origin',(0.,-0.25,0.));
#49578=CARTESIAN_POINT('Origin',(0.22,0.,0.));
#49579=CARTESIAN_POINT('',(-0.22,-8.67361737988404E-18,-2.69422295812418E-17));
#49580=CARTESIAN_POINT('Origin',(0.,0.,0.));
#49581=CARTESIAN_POINT('Origin',(0.,-0.015,0.));
#49582=CARTESIAN_POINT('',(-0.24505,-0.02505,-3.00099698131059E-17));
#49583=CARTESIAN_POINT('Origin',(0.,-0.02505,0.));
#49584=CARTESIAN_POINT('',(-0.235,-0.015,-2.87791997799628E-17));
#49585=CARTESIAN_POINT('Origin',(0.,-0.3775,0.));
#49586=CARTESIAN_POINT('',(-0.24505,-0.72995,3.00099698131059E-17));
#49587=CARTESIAN_POINT('Origin',(0.,-0.72995,0.));
#49588=CARTESIAN_POINT('',(-0.24505,-0.3775,-3.00099698131059E-17));
#49589=CARTESIAN_POINT('Origin',(0.,-0.7625,0.));
#49590=CARTESIAN_POINT('',(-0.175,-0.8,-2.14313189850787E-17));
#49591=CARTESIAN_POINT('Origin',(0.,-0.8,0.));
#49592=CARTESIAN_POINT('',(-0.2125,-0.7625,-2.60237444818813E-17));
#49593=CARTESIAN_POINT('Origin',(0.,-0.8,0.));
#73299=UNCERTAINTY_MEASURE_WITH_UNIT(LENGTH_MEASURE(0.001),#73367,
'DISTANCE_ACCURACY_VALUE',
'Maximum model space distance between geometric entities at asserted c
onnectivities');
#73302=UNCERTAINTY_MEASURE_WITH_UNIT(LENGTH_MEASURE(0.001),#73367,
'DISTANCE_ACCURACY_VALUE',
'Maximum model space distance between geometric entities at asserted c
onnectivities');
#73363=(
GEOMETRIC_REPRESENTATION_CONTEXT(3)
GLOBAL_UNCERTAINTY_ASSIGNED_CONTEXT((#73299))
GLOBAL_UNIT_ASSIGNED_CONTEXT((#73367,#73369,#73370))
REPRESENTATION_CONTEXT('','3D')
);
#73366=(
GEOMETRIC_REPRESENTATION_CONTEXT(3)
GLOBAL_UNCERTAINTY_ASSIGNED_CONTEXT((#73302))
GLOBAL_UNIT_ASSIGNED_CONTEXT((#73367,#73369,#73370))
REPRESENTATION_CONTEXT('','3D')
);
#73367=(
LENGTH_UNIT()
NAMED_UNIT(*)
SI_UNIT(.CENTI.,.METRE.)
);
#73369=(
NAMED_UNIT(*)
PLANE_ANGLE_UNIT()
SI_UNIT($,.RADIAN.)
);
#73370=(
NAMED_UNIT(*)
SI_UNIT($,.STERADIAN.)
SOLID_ANGLE_UNIT()
);
#73431=SHAPE_DEFINITION_REPRESENTATION(#73564,#73667);
#73564=PRODUCT_DEFINITION_SHAPE('',$,#73731);
#73667=SHAPE_REPRESENTATION('',(#18217),#73363);
#73670=PRODUCT_DEFINITION_CONTEXT('part definition',#73861,'design');
#73731=PRODUCT_DEFINITION('Socket Set Screw - M5x8',
'Socket Set Screw - M5x8',#73794,#73670);
#73794=PRODUCT_DEFINITION_FORMATION('',$,#73923);
#73861=APPLICATION_CONTEXT(
'Core Data for Automotive Mechanical Design Process');
#73862=PRODUCT_CONTEXT('part definition',#73861,'mechanical');
#73923=PRODUCT('Socket Set Screw - M5x8','Socket Set Screw - M5x8',
'Socket Set Screw - M5x8',(#73862));
#73989=COLOUR_RGB('Black',0.12,0.14,0.17);
#73990=FILL_AREA_STYLE_COLOUR('',#73989);
#73991=FILL_AREA_STYLE('',(#73990));
#73992=SURFACE_STYLE_FILL_AREA(#73991);
#73993=SURFACE_SIDE_STYLE('',(#73992));
#73994=SURFACE_STYLE_USAGE(.BOTH.,#73993);
#73995=PRESENTATION_STYLE_ASSIGNMENT((#73994));
ENDSEC;
END-ISO-10303-21;
